ISO-10303-21;
HEADER;
/* Generated by software containing ST-Developer
 * from STEP Tools, Inc. (www.steptools.com) 
 */

FILE_DESCRIPTION(
/* description */ ('Manual rail carriage with stops'),
/* implementation_level */ '2;1');

FILE_NAME(
/* name */ 'Flat Washer - M6.step',
/* time_stamp */ '2026-10-27T18:54:27-07:00',
/* author */ (''),
/* organization */ (''),
/* preprocessor_version */ 'ST-DEVELOPER v20.2',
/* originating_system */ 'Autodesk Translation Framework v15.17.0.0',
/* authorisation */ '');

FILE_SCHEMA (('AUTOMOTIVE_DESIGN { 1 0 10303 214 3 1 1 }'));
ENDSEC;

DATA;
#10=MECHANICAL_DESIGN_GEOMETRIC_PRESENTATION_REPRESENTATION('',(#289),#8499);
#253=SHAPE_REPRESENTATION_RELATIONSHIP('SRR','None',#8618,#271);
#271=ADVANCED_BREP_SHAPE_REPRESENTATION('',(#304),#8497);
#289=STYLED_ITEM('',(#8795),#304);
#304=MANIFOLD_SOLID_BREP('Body1',#4960);
#377=FACE_BOUND('',#1161,.T.);
#378=FACE_BOUND('',#1163,.T.);
#564=PLANE('',#5588);
#565=PLANE('',#5589);
#821=FACE_OUTER_BOUND('',#1158,.T.);
#822=FACE_OUTER_BOUND('',#1159,.T.);
#823=FACE_OUTER_BOUND('',#1160,.T.);
#824=FACE_OUTER_BOUND('',#1162,.T.);
#1158=EDGE_LOOP('',(#4548,#4549,#4550,#4551));
#1159=EDGE_LOOP('',(#4552,#4553,#4554,#4555));
#1160=EDGE_LOOP('',(#4556));
#1161=EDGE_LOOP('',(#4557));
#1162=EDGE_LOOP('',(#4558));
#1163=EDGE_LOOP('',(#4559));
#1656=LINE('',#8359,#2156);
#1657=LINE('',#8365,#2157);
#2156=VECTOR('',#6949,0.32);
#2157=VECTOR('',#6956,0.6);
#2300=CIRCLE('',#5583,0.32);
#2301=CIRCLE('',#5584,0.32);
#2302=CIRCLE('',#5586,0.6);
#2303=CIRCLE('',#5587,0.6);
#2704=VERTEX_POINT('',#8356);
#2705=VERTEX_POINT('',#8358);
#2706=VERTEX_POINT('',#8362);
#2707=VERTEX_POINT('',#8364);
#3322=EDGE_CURVE('',#2704,#2704,#2300,.T.);
#3323=EDGE_CURVE('',#2704,#2705,#1656,.T.);
#3324=EDGE_CURVE('',#2705,#2705,#2301,.T.);
#3325=EDGE_CURVE('',#2706,#2706,#2302,.T.);
#3326=EDGE_CURVE('',#2706,#2707,#1657,.T.);
#3327=EDGE_CURVE('',#2707,#2707,#2303,.T.);
#4548=ORIENTED_EDGE('',*,*,#3322,.F.);
#4549=ORIENTED_EDGE('',*,*,#3323,.T.);
#4550=ORIENTED_EDGE('',*,*,#3324,.T.);
#4551=ORIENTED_EDGE('',*,*,#3323,.F.);
#4552=ORIENTED_EDGE('',*,*,#3325,.F.);
#4553=ORIENTED_EDGE('',*,*,#3326,.T.);
#4554=ORIENTED_EDGE('',*,*,#3327,.T.);
#4555=ORIENTED_EDGE('',*,*,#3326,.F.);
#4556=ORIENTED_EDGE('',*,*,#3325,.T.);
#4557=ORIENTED_EDGE('',*,*,#3322,.T.);
#4558=ORIENTED_EDGE('',*,*,#3327,.F.);
#4559=ORIENTED_EDGE('',*,*,#3324,.F.);
#4672=CYLINDRICAL_SURFACE('',#5582,0.32);
#4673=CYLINDRICAL_SURFACE('',#5585,0.6);
#4920=ADVANCED_FACE('',(#821),#4672,.F.);
#4921=ADVANCED_FACE('',(#822),#4673,.T.);
#4922=ADVANCED_FACE('',(#823,#377),#564,.T.);
#4923=ADVANCED_FACE('',(#824,#378),#565,.F.);
#4960=CLOSED_SHELL('',(#4920,#4921,#4922,#4923));
#5581=AXIS2_PLACEMENT_3D('',#8354,#6943,#6944);
#5582=AXIS2_PLACEMENT_3D('',#8355,#6945,#6946);
#5583=AXIS2_PLACEMENT_3D('',#8357,#6947,#6948);
#5584=AXIS2_PLACEMENT_3D('',#8360,#6950,#6951);
#5585=AXIS2_PLACEMENT_3D('',#8361,#6952,#6953);
#5586=AXIS2_PLACEMENT_3D('',#8363,#6954,#6955);
#5587=AXIS2_PLACEMENT_3D('',#8366,#6957,#6958);
#5588=AXIS2_PLACEMENT_3D('',#8367,#6959,#6960);
#5589=AXIS2_PLACEMENT_3D('',#8368,#6961,#6962);
#6943=DIRECTION('axis',(0.,0.,1.));
#6944=DIRECTION('refdir',(1.,0.,0.));
#6945=DIRECTION('center_axis',(0.,1.,0.));
#6946=DIRECTION('ref_axis',(1.,0.,0.));
#6947=DIRECTION('center_axis',(0.,-1.,0.));
#6948=DIRECTION('ref_axis',(1.,0.,0.));
#6949=DIRECTION('',(0.,-1.,0.));
#6950=DIRECTION('center_axis',(0.,-1.,0.));
#6951=DIRECTION('ref_axis',(1.,0.,0.));
#6952=DIRECTION('center_axis',(0.,1.,0.));
#6953=DIRECTION('ref_axis',(1.,0.,0.));
#6954=DIRECTION('center_axis',(0.,1.,0.));
#6955=DIRECTION('ref_axis',(1.,0.,0.));
#6956=DIRECTION('',(0.,-1.,0.));
#6957=DIRECTION('center_axis',(0.,1.,0.));
#6958=DIRECTION('ref_axis',(1.,0.,0.));
#6959=DIRECTION('center_axis',(0.,1.,0.));
#6960=DIRECTION('ref_axis',(1.,0.,0.));
#6961=DIRECTION('center_axis',(0.,1.,0.));
#6962=DIRECTION('ref_axis',(1.,0.,0.));
#8354=CARTESIAN_POINT('',(0.,0.,0.));
#8355=CARTESIAN_POINT('Origin',(0.,0.,0.));
#8356=CARTESIAN_POINT('',(-0.32,0.16,3.91886975727153E-17));
#8357=CARTESIAN_POINT('Origin',(0.,0.16,0.));
#8358=CARTESIAN_POINT('',(-0.32,0.,3.91886975727153E-17));
#8359=CARTESIAN_POINT('',(-0.32,0.,3.91886975727153E-17));
#8360=CARTESIAN_POINT('Origin',(0.,0.,0.));
#8361=CARTESIAN_POINT('Origin',(0.,0.,0.));
#8362=CARTESIAN_POINT('',(-0.6,0.16,7.34788079488412E-17));
#8363=CARTESIAN_POINT('Origin',(0.,0.16,0.));
#8364=CARTESIAN_POINT('',(-0.6,0.,7.34788079488412E-17));
#8365=CARTESIAN_POINT('',(-0.6,0.,7.34788079488412E-17));
#8366=CARTESIAN_POINT('Origin',(0.,0.,0.));
#8367=CARTESIAN_POINT('Origin',(0.,0.16,0.));
#8368=CARTESIAN_POINT('Origin',(0.,0.,0.));
#8474=UNCERTAINTY_MEASURE_WITH_UNIT(LENGTH_MEASURE(0.001),#8500,
'DISTANCE_ACCURACY_VALUE',
'Maximum model space distance between geometric entities at asserted c
onnectivities');
#8476=UNCERTAINTY_MEASURE_WITH_UNIT(LENGTH_MEASURE(0.001),#8500,
'DISTANCE_ACCURACY_VALUE',
'Maximum model space distance between geometric entities at asserted c
onnectivities');
#8497=(
GEOMETRIC_REPRESENTATION_CONTEXT(3)
GLOBAL_UNCERTAINTY_ASSIGNED_CONTEXT((#8474))
GLOBAL_UNIT_ASSIGNED_CONTEXT((#8500,#8502,#8503))
REPRESENTATION_CONTEXT('','3D')
);
#8499=(
GEOMETRIC_REPRESENTATION_CONTEXT(3)
GLOBAL_UNCERTAINTY_ASSIGNED_CONTEXT((#8476))
GLOBAL_UNIT_ASSIGNED_CONTEXT((#8500,#8502,#8503))
REPRESENTATION_CONTEXT('','3D')
);
#8500=(
LENGTH_UNIT()
NAMED_UNIT(*)
SI_UNIT(.CENTI.,.METRE.)
);
#8502=(
NAMED_UNIT(*)
PLANE_ANGLE_UNIT()
SI_UNIT($,.RADIAN.)
);
#8503=(
NAMED_UNIT(*)
SI_UNIT($,.STERADIAN.)
SOLID_ANGLE_UNIT()
);
#8524=SHAPE_DEFINITION_REPRESENTATION(#8581,#8618);
#8581=PRODUCT_DEFINITION_SHAPE('',$,#8641);
#8618=SHAPE_REPRESENTATION('',(#5581),#8497);
#8620=PRODUCT_DEFINITION_CONTEXT('part definition',#8688,'design');
#8641=PRODUCT_DEFINITION('Flat Washer - M6','Flat Washer - M6',#8663,#8620);
#8663=PRODUCT_DEFINITION_FORMATION('',$,#8710);
#8688=APPLICATION_CONTEXT(
'Core Data for Automotive Mechanical Design Process');
#8689=PRODUCT_CONTEXT('part definition',#8688,'mechanical');
#8710=PRODUCT('Flat Washer - M6','Flat Washer - M6','Flat Washer - M6',
(#8689));
#8789=COLOUR_RGB('Black',0.12,0.14,0.17);
#8790=FILL_AREA_STYLE_COLOUR('',#8789);
#8791=FILL_AREA_STYLE('',(#8790));
#8792=SURFACE_STYLE_FILL_AREA(#8791);
#8793=SURFACE_SIDE_STYLE('',(#8792));
#8794=SURFACE_STYLE_USAGE(.BOTH.,#8793);
#8795=PRESENTATION_STYLE_ASSIGNMENT((#8794));
ENDSEC;
END-ISO-10303-21;
